ISO-10303-21;
HEADER;
/* Generated by software containing ST-Developer
 * from STEP Tools, Inc. (www.steptools.com) 
 */

FILE_DESCRIPTION(
/* description */ ('Ball-race swivel caster'),
/* implementation_level */ '2;1');

FILE_NAME(
/* name */ 'Balls (1).step',
/* time_stamp */ '2026-10-29T16:15:51-07:00',
/* author */ (''),
/* organization */ (''),
/* preprocessor_version */ 'ST-DEVELOPER v20.2',
/* originating_system */ 'Autodesk Translation Framework v15.17.0.0',
/* authorisation */ '');

FILE_SCHEMA (('AUTOMOTIVE_DESIGN { 1 0 10303 214 3 1 1 }'));
ENDSEC;

DATA;
#10=MECHANICAL_DESIGN_GEOMETRIC_PRESENTATION_REPRESENTATION('',(#323,#324,#325,#326,#327,#328,#329),#7816);
#156=SPHERICAL_SURFACE('',#4386,0.29765);
#157=SPHERICAL_SURFACE('',#4388,0.29765);
#158=SPHERICAL_SURFACE('',#4390,0.29765);
#159=SPHERICAL_SURFACE('',#4392,0.29765);
#160=SPHERICAL_SURFACE('',#4394,0.29765);
#161=SPHERICAL_SURFACE('',#4396,0.29765);
#162=SPHERICAL_SURFACE('',#4398,0.29765);
#274=SHAPE_REPRESENTATION_RELATIONSHIP('SRR','None',#7923,#294);
#294=ADVANCED_BREP_SHAPE_REPRESENTATION('',(#358,#359,#360,#361,#362,#363,
#364),#7812);
#323=STYLED_ITEM('',(#8097),#358);
#324=STYLED_ITEM('',(#8097),#359);
#325=STYLED_ITEM('',(#8097),#360);
#326=STYLED_ITEM('',(#8097),#361);
#327=STYLED_ITEM('',(#8097),#362);
#328=STYLED_ITEM('',(#8097),#363);
#329=STYLED_ITEM('',(#8097),#364);
#358=MANIFOLD_SOLID_BREP('Body1',#3730);
#359=MANIFOLD_SOLID_BREP('Body2',#3731);
#360=MANIFOLD_SOLID_BREP('Body3',#3732);
#361=MANIFOLD_SOLID_BREP('Body4',#3733);
#362=MANIFOLD_SOLID_BREP('Body5',#3734);
#363=MANIFOLD_SOLID_BREP('Body6',#3735);
#364=MANIFOLD_SOLID_BREP('Body7',#3736);
#697=FACE_OUTER_BOUND('',#968,.T.);
#698=FACE_OUTER_BOUND('',#969,.T.);
#699=FACE_OUTER_BOUND('',#970,.T.);
#700=FACE_OUTER_BOUND('',#971,.T.);
#701=FACE_OUTER_BOUND('',#972,.T.);
#702=FACE_OUTER_BOUND('',#973,.T.);
#703=FACE_OUTER_BOUND('',#974,.T.);
#968=EDGE_LOOP('',(#3281,#3282));
#969=EDGE_LOOP('',(#3283,#3284));
#970=EDGE_LOOP('',(#3285,#3286));
#971=EDGE_LOOP('',(#3287,#3288));
#972=EDGE_LOOP('',(#3289,#3290));
#973=EDGE_LOOP('',(#3291,#3292));
#974=EDGE_LOOP('',(#3293,#3294));
#1534=CIRCLE('',#4387,0.29765);
#1535=CIRCLE('',#4389,0.29765);
#1536=CIRCLE('',#4391,0.29765);
#1537=CIRCLE('',#4393,0.29765);
#1538=CIRCLE('',#4395,0.29765);
#1539=CIRCLE('',#4397,0.29765);
#1540=CIRCLE('',#4399,0.29765);
#1878=VERTEX_POINT('',#7287);
#1879=VERTEX_POINT('',#7288);
#1880=VERTEX_POINT('',#7291);
#1881=VERTEX_POINT('',#7292);
#1882=VERTEX_POINT('',#7295);
#1883=VERTEX_POINT('',#7296);
#1884=VERTEX_POINT('',#7299);
#1885=VERTEX_POINT('',#7300);
#1886=VERTEX_POINT('',#7303);
#1887=VERTEX_POINT('',#7304);
#1888=VERTEX_POINT('',#7307);
#1889=VERTEX_POINT('',#7308);
#1890=VERTEX_POINT('',#7311);
#1891=VERTEX_POINT('',#7312);
#2360=EDGE_CURVE('',#1878,#1879,#1534,.T.);
#2361=EDGE_CURVE('',#1880,#1881,#1535,.T.);
#2362=EDGE_CURVE('',#1882,#1883,#1536,.T.);
#2363=EDGE_CURVE('',#1884,#1885,#1537,.T.);
#2364=EDGE_CURVE('',#1886,#1887,#1538,.T.);
#2365=EDGE_CURVE('',#1888,#1889,#1539,.T.);
#2366=EDGE_CURVE('',#1890,#1891,#1540,.T.);
#3281=ORIENTED_EDGE('',*,*,#2360,.T.);
#3282=ORIENTED_EDGE('',*,*,#2360,.F.);
#3283=ORIENTED_EDGE('',*,*,#2361,.T.);
#3284=ORIENTED_EDGE('',*,*,#2361,.F.);
#3285=ORIENTED_EDGE('',*,*,#2362,.T.);
#3286=ORIENTED_EDGE('',*,*,#2362,.F.);
#3287=ORIENTED_EDGE('',*,*,#2363,.T.);
#3288=ORIENTED_EDGE('',*,*,#2363,.F.);
#3289=ORIENTED_EDGE('',*,*,#2364,.T.);
#3290=ORIENTED_EDGE('',*,*,#2364,.F.);
#3291=ORIENTED_EDGE('',*,*,#2365,.T.);
#3292=ORIENTED_EDGE('',*,*,#2365,.F.);
#3293=ORIENTED_EDGE('',*,*,#2366,.T.);
#3294=ORIENTED_EDGE('',*,*,#2366,.F.);
#3668=ADVANCED_FACE('',(#697),#156,.T.);
#3669=ADVANCED_FACE('',(#698),#157,.T.);
#3670=ADVANCED_FACE('',(#699),#158,.T.);
#3671=ADVANCED_FACE('',(#700),#159,.T.);
#3672=ADVANCED_FACE('',(#701),#160,.T.);
#3673=ADVANCED_FACE('',(#702),#161,.T.);
#3674=ADVANCED_FACE('',(#703),#162,.T.);
#3730=CLOSED_SHELL('',(#3668));
#3731=CLOSED_SHELL('',(#3669));
#3732=CLOSED_SHELL('',(#3670));
#3733=CLOSED_SHELL('',(#3671));
#3734=CLOSED_SHELL('',(#3672));
#3735=CLOSED_SHELL('',(#3673));
#3736=CLOSED_SHELL('',(#3674));
#4385=AXIS2_PLACEMENT_3D('',#7285,#5482,#5483);
#4386=AXIS2_PLACEMENT_3D('',#7286,#5484,#5485);
#4387=AXIS2_PLACEMENT_3D('',#7289,#5486,#5487);
#4388=AXIS2_PLACEMENT_3D('',#7290,#5488,#5489);
#4389=AXIS2_PLACEMENT_3D('',#7293,#5490,#5491);
#4390=AXIS2_PLACEMENT_3D('',#7294,#5492,#5493);
#4391=AXIS2_PLACEMENT_3D('',#7297,#5494,#5495);
#4392=AXIS2_PLACEMENT_3D('',#7298,#5496,#5497);
#4393=AXIS2_PLACEMENT_3D('',#7301,#5498,#5499);
#4394=AXIS2_PLACEMENT_3D('',#7302,#5500,#5501);
#4395=AXIS2_PLACEMENT_3D('',#7305,#5502,#5503);
#4396=AXIS2_PLACEMENT_3D('',#7306,#5504,#5505);
#4397=AXIS2_PLACEMENT_3D('',#7309,#5506,#5507);
#4398=AXIS2_PLACEMENT_3D('',#7310,#5508,#5509);
#4399=AXIS2_PLACEMENT_3D('',#7313,#5510,#5511);
#5482=DIRECTION('axis',(0.,0.,1.));
#5483=DIRECTION('refdir',(1.,0.,0.));
#5484=DIRECTION('center_axis',(0.,0.,1.));
#5485=DIRECTION('ref_axis',(1.,0.,0.));
#5486=DIRECTION('center_axis',(1.22464679914735E-16,-1.,0.));
#5487=DIRECTION('ref_axis',(-1.,-1.22464679914735E-16,0.));
#5488=DIRECTION('center_axis',(0.78183148246803,0.,0.623489801858733));
#5489=DIRECTION('ref_axis',(0.623489801858734,0.,-0.78183148246803));
#5490=DIRECTION('center_axis',(7.63554790147315E-17,-1.,-9.57467422477103E-17));
#5491=DIRECTION('ref_axis',(-0.623489801858734,-1.22464679914735E-16,0.78183148246803));
#5492=DIRECTION('center_axis',(0.974927912181824,0.,-0.222520933956314));
#5493=DIRECTION('ref_axis',(-0.222520933956314,0.,-0.974927912181824));
#5494=DIRECTION('center_axis',(-2.7250954951288E-17,-1.,-1.19394234705288E-16));
#5495=DIRECTION('ref_axis',(0.222520933956314,-1.22464679914735E-16,0.974927912181824));
#5496=DIRECTION('center_axis',(0.433883739117558,0.,-0.900968867902419));
#5497=DIRECTION('ref_axis',(-0.900968867902419,0.,-0.433883739117558));
#5498=DIRECTION('center_axis',(-1.10336864020811E-16,-1.,-5.31354332312403E-17));
#5499=DIRECTION('ref_axis',(0.900968867902419,-1.22464679914735E-16,0.433883739117558));
#5500=DIRECTION('center_axis',(-0.433883739117558,0.,-0.900968867902419));
#5501=DIRECTION('ref_axis',(-0.900968867902419,0.,0.433883739117558));
#5502=DIRECTION('center_axis',(-1.10336864020811E-16,-1.,5.31354332312403E-17));
#5503=DIRECTION('ref_axis',(0.900968867902419,-1.22464679914735E-16,-0.433883739117558));
#5504=DIRECTION('center_axis',(-0.974927912181824,0.,-0.222520933956314));
#5505=DIRECTION('ref_axis',(-0.222520933956315,0.,0.974927912181824));
#5506=DIRECTION('center_axis',(-2.7250954951288E-17,-1.,1.19394234705288E-16));
#5507=DIRECTION('ref_axis',(0.222520933956315,-1.22464679914735E-16,-0.974927912181824));
#5508=DIRECTION('center_axis',(-0.78183148246803,0.,0.623489801858734));
#5509=DIRECTION('ref_axis',(0.623489801858733,0.,0.78183148246803));
#5510=DIRECTION('center_axis',(7.63554790147315E-17,-1.,9.57467422477103E-17));
#5511=DIRECTION('ref_axis',(-0.623489801858733,-1.22464679914735E-16,-0.78183148246803));
#7285=CARTESIAN_POINT('',(0.,0.,0.));
#7286=CARTESIAN_POINT('Origin',(1.1,0.,0.));
#7287=CARTESIAN_POINT('',(1.1,-2.23201749654651E-33,0.29765));
#7288=CARTESIAN_POINT('',(1.1,-2.23201749654651E-33,-0.29765));
#7289=CARTESIAN_POINT('Origin',(1.1,0.,0.));
#7290=CARTESIAN_POINT('Origin',(0.685838782044607,0.,-0.860014630714833));
#7291=CARTESIAN_POINT('',(0.918550922801216,-5.31350540756609E-33,-0.674432891191581));
#7292=CARTESIAN_POINT('',(0.453126641287998,8.49470414473068E-34,-1.04559637023808));
#7293=CARTESIAN_POINT('Origin',(0.685838782044607,0.,-0.860014630714833));
#7294=CARTESIAN_POINT('Origin',(-0.244773027351946,0.,-1.07242070340001));
#7295=CARTESIAN_POINT('',(0.0454142657089739,-2.23201749654651E-33,-1.1386540593921));
#7296=CARTESIAN_POINT('',(-0.534960320412865,-2.23201749654651E-33,-1.00618734740791));
#7297=CARTESIAN_POINT('Origin',(-0.244773027351946,0.,-1.07242070340001));
#7298=CARTESIAN_POINT('Origin',(-0.991065754692661,0.,-0.477272113029314));
#7299=CARTESIAN_POINT('',(-0.86192025974432,8.49470414473067E-34,-0.745445496560469));
#7300=CARTESIAN_POINT('',(-1.120211249641,-5.31350540756609E-33,-0.209098729498159));
#7301=CARTESIAN_POINT('Origin',(-0.991065754692661,0.,-0.477272113029314));
#7302=CARTESIAN_POINT('Origin',(-0.991065754692661,0.,0.477272113029314));
#7303=CARTESIAN_POINT('',(-1.120211249641,-2.23201749654651E-33,0.209098729498159));
#7304=CARTESIAN_POINT('',(-0.86192025974432,-2.23201749654651E-33,0.745445496560469));
#7305=CARTESIAN_POINT('Origin',(-0.991065754692661,0.,0.477272113029314));
#7306=CARTESIAN_POINT('Origin',(-0.244773027351946,0.,1.07242070340001));
#7307=CARTESIAN_POINT('',(-0.534960320412866,-2.23201749654651E-33,1.00618734740791));
#7308=CARTESIAN_POINT('',(0.0454142657089737,-2.23201749654651E-33,1.1386540593921));
#7309=CARTESIAN_POINT('Origin',(-0.244773027351946,0.,1.07242070340001));
#7310=CARTESIAN_POINT('Origin',(0.685838782044607,0.,0.860014630714833));
#7311=CARTESIAN_POINT('',(0.453126641287998,-2.23201749654651E-33,1.04559637023808));
#7312=CARTESIAN_POINT('',(0.918550922801216,-2.23201749654651E-33,0.674432891191581));
#7313=CARTESIAN_POINT('Origin',(0.685838782044607,0.,0.860014630714833));
#7785=UNCERTAINTY_MEASURE_WITH_UNIT(LENGTH_MEASURE(0.001),#7817,
'DISTANCE_ACCURACY_VALUE',
'Maximum model space distance between geometric entities at asserted c
onnectivities');
#7789=UNCERTAINTY_MEASURE_WITH_UNIT(LENGTH_MEASURE(0.001),#7817,
'DISTANCE_ACCURACY_VALUE',
'Maximum model space distance between geometric entities at asserted c
onnectivities');
#7812=(
GEOMETRIC_REPRESENTATION_CONTEXT(3)
GLOBAL_UNCERTAINTY_ASSIGNED_CONTEXT((#7785))
GLOBAL_UNIT_ASSIGNED_CONTEXT((#7817,#7819,#7820))
REPRESENTATION_CONTEXT('','3D')
);
#7816=(
GEOMETRIC_REPRESENTATION_CONTEXT(3)
GLOBAL_UNCERTAINTY_ASSIGNED_CONTEXT((#7789))
GLOBAL_UNIT_ASSIGNED_CONTEXT((#7817,#7819,#7820))
REPRESENTATION_CONTEXT('','3D')
);
#7817=(
LENGTH_UNIT()
NAMED_UNIT(*)
SI_UNIT(.CENTI.,.METRE.)
);
#7819=(
NAMED_UNIT(*)
PLANE_ANGLE_UNIT()
SI_UNIT($,.RADIAN.)
);
#7820=(
NAMED_UNIT(*)
SI_UNIT($,.STERADIAN.)
SOLID_ANGLE_UNIT()
);
#7843=SHAPE_DEFINITION_REPRESENTATION(#7884,#7923);
#7884=PRODUCT_DEFINITION_SHAPE('',$,#7950);
#7923=SHAPE_REPRESENTATION('',(#4385),#7812);
#7927=PRODUCT_DEFINITION_CONTEXT('part definition',#8007,'design');
#7950=PRODUCT_DEFINITION('Balls (1)','Balls (1)',#7976,#7927);
#7976=PRODUCT_DEFINITION_FORMATION('',$,#8031);
#8007=APPLICATION_CONTEXT(
'Core Data for Automotive Mechanical Design Process');
#8008=PRODUCT_CONTEXT('part definition',#8007,'mechanical');
#8031=PRODUCT('Balls (1)','Balls (1)','Balls (1)',(#8008));
#8091=COLOUR_RGB('Grey',0.48,0.52,0.57);
#8092=FILL_AREA_STYLE_COLOUR('',#8091);
#8093=FILL_AREA_STYLE('',(#8092));
#8094=SURFACE_STYLE_FILL_AREA(#8093);
#8095=SURFACE_SIDE_STYLE('',(#8094));
#8096=SURFACE_STYLE_USAGE(.BOTH.,#8095);
#8097=PRESENTATION_STYLE_ASSIGNMENT((#8096));
ENDSEC;
END-ISO-10303-21;
